ISO-10303-21;
HEADER;
/* Generated by software containing ST-Developer
 * from STEP Tools, Inc. (www.steptools.com) 
 */

FILE_DESCRIPTION(
/* description */ ('Compact handwheel screw vise'),
/* implementation_level */ '2;1');

FILE_NAME(
/* name */ 'Seventy-five millimetre jaw insert (1).step',
/* time_stamp */ '2026-10-29T16:08:22-07:00',
/* author */ (''),
/* organization */ (''),
/* preprocessor_version */ 'ST-DEVELOPER v20.2',
/* originating_system */ 'Autodesk Translation Framework v15.17.0.0',
/* authorisation */ '');

FILE_SCHEMA (('AUTOMOTIVE_DESIGN { 1 0 10303 214 3 1 1 }'));
ENDSEC;

DATA;
#10=MECHANICAL_DESIGN_GEOMETRIC_PRESENTATION_REPRESENTATION('',(#666),#25074);
#602=SHAPE_REPRESENTATION_RELATIONSHIP('SRR','None',#25212,#630);
#630=ADVANCED_BREP_SHAPE_REPRESENTATION('',(#701),#25059);
#666=STYLED_ITEM('',(#25453),#701);
#701=MANIFOLD_SOLID_BREP('Body1',#8075);
#782=FACE_BOUND('',#1731,.T.);
#783=FACE_BOUND('',#1732,.T.);
#784=FACE_BOUND('',#1736,.T.);
#785=FACE_BOUND('',#1737,.T.);
#786=FACE_BOUND('',#1740,.T.);
#787=FACE_BOUND('',#1743,.T.);
#919=PLANE('',#8763);
#920=PLANE('',#8764);
#921=PLANE('',#8767);
#922=PLANE('',#8768);
#923=PLANE('',#8769);
#924=PLANE('',#8774);
#925=PLANE('',#8778);
#926=PLANE('',#8782);
#1189=FACE_OUTER_BOUND('',#1729,.T.);
#1190=FACE_OUTER_BOUND('',#1730,.T.);
#1191=FACE_OUTER_BOUND('',#1733,.T.);
#1192=FACE_OUTER_BOUND('',#1734,.T.);
#1193=FACE_OUTER_BOUND('',#1735,.T.);
#1194=FACE_OUTER_BOUND('',#1738,.T.);
#1195=FACE_OUTER_BOUND('',#1739,.T.);
#1196=FACE_OUTER_BOUND('',#1741,.T.);
#1197=FACE_OUTER_BOUND('',#1742,.T.);
#1198=FACE_OUTER_BOUND('',#1744,.T.);
#1199=FACE_OUTER_BOUND('',#1745,.T.);
#1200=FACE_OUTER_BOUND('',#1746,.T.);
#1729=EDGE_LOOP('',(#5875,#5876,#5877,#5878));
#1730=EDGE_LOOP('',(#5879,#5880,#5881,#5882));
#1731=EDGE_LOOP('',(#5883));
#1732=EDGE_LOOP('',(#5884));
#1733=EDGE_LOOP('',(#5885,#5886,#5887,#5888));
#1734=EDGE_LOOP('',(#5889,#5890,#5891,#5892));
#1735=EDGE_LOOP('',(#5893,#5894,#5895,#5896));
#1736=EDGE_LOOP('',(#5897));
#1737=EDGE_LOOP('',(#5898));
#1738=EDGE_LOOP('',(#5899,#5900,#5901,#5902));
#1739=EDGE_LOOP('',(#5903));
#1740=EDGE_LOOP('',(#5904));
#1741=EDGE_LOOP('',(#5905,#5906,#5907,#5908));
#1742=EDGE_LOOP('',(#5909));
#1743=EDGE_LOOP('',(#5910));
#1744=EDGE_LOOP('',(#5911,#5912,#5913,#5914));
#1745=EDGE_LOOP('',(#5915,#5916,#5917,#5918));
#1746=EDGE_LOOP('',(#5919,#5920,#5921,#5922));
#2241=LINE('',#12465,#2749);
#2242=LINE('',#12467,#2750);
#2243=LINE('',#12469,#2751);
#2244=LINE('',#12470,#2752);
#2245=LINE('',#12473,#2753);
#2246=LINE('',#12475,#2754);
#2247=LINE('',#12476,#2755);
#2248=LINE('',#12483,#2756);
#2249=LINE('',#12484,#2757);
#2250=LINE('',#12487,#2758);
#2251=LINE('',#12488,#2759);
#2252=LINE('',#12490,#2760);
#2253=LINE('',#12497,#2761);
#2254=LINE('',#12504,#2762);
#2255=LINE('',#12510,#2763);
#2256=LINE('',#12512,#2764);
#2749=VECTOR('',#10109,1.);
#2750=VECTOR('',#10110,1.);
#2751=VECTOR('',#10111,1.);
#2752=VECTOR('',#10112,1.);
#2753=VECTOR('',#10115,1.);
#2754=VECTOR('',#10116,1.);
#2755=VECTOR('',#10117,1.);
#2756=VECTOR('',#10124,1.);
#2757=VECTOR('',#10125,1.);
#2758=VECTOR('',#10128,1.);
#2759=VECTOR('',#10129,1.);
#2760=VECTOR('',#10132,1.);
#2761=VECTOR('',#10139,0.475);
#2762=VECTOR('',#10148,0.475);
#2763=VECTOR('',#10157,0.275);
#2764=VECTOR('',#10160,0.275);
#3239=CIRCLE('',#8765,0.475);
#3240=CIRCLE('',#8766,0.475);
#3241=CIRCLE('',#8770,0.275);
#3242=CIRCLE('',#8771,0.275);
#3243=CIRCLE('',#8773,0.475);
#3244=CIRCLE('',#8775,0.275);
#3245=CIRCLE('',#8777,0.475);
#3246=CIRCLE('',#8779,0.275);
#3580=VERTEX_POINT('',#12463);
#3581=VERTEX_POINT('',#12464);
#3582=VERTEX_POINT('',#12466);
#3583=VERTEX_POINT('',#12468);
#3584=VERTEX_POINT('',#12472);
#3585=VERTEX_POINT('',#12474);
#3586=VERTEX_POINT('',#12477);
#3587=VERTEX_POINT('',#12479);
#3588=VERTEX_POINT('',#12482);
#3589=VERTEX_POINT('',#12486);
#3590=VERTEX_POINT('',#12491);
#3591=VERTEX_POINT('',#12493);
#3592=VERTEX_POINT('',#12496);
#3593=VERTEX_POINT('',#12500);
#3594=VERTEX_POINT('',#12503);
#3595=VERTEX_POINT('',#12507);
#4424=EDGE_CURVE('',#3580,#3581,#2241,.T.);
#4425=EDGE_CURVE('',#3582,#3580,#2242,.T.);
#4426=EDGE_CURVE('',#3583,#3582,#2243,.T.);
#4427=EDGE_CURVE('',#3581,#3583,#2244,.T.);
#4428=EDGE_CURVE('',#3582,#3584,#2245,.T.);
#4429=EDGE_CURVE('',#3584,#3585,#2246,.T.);
#4430=EDGE_CURVE('',#3583,#3585,#2247,.T.);
#4431=EDGE_CURVE('',#3586,#3586,#3239,.T.);
#4432=EDGE_CURVE('',#3587,#3587,#3240,.T.);
#4433=EDGE_CURVE('',#3588,#3580,#2248,.T.);
#4434=EDGE_CURVE('',#3588,#3584,#2249,.T.);
#4435=EDGE_CURVE('',#3589,#3588,#2250,.T.);
#4436=EDGE_CURVE('',#3585,#3589,#2251,.T.);
#4437=EDGE_CURVE('',#3589,#3581,#2252,.T.);
#4438=EDGE_CURVE('',#3590,#3590,#3241,.T.);
#4439=EDGE_CURVE('',#3591,#3591,#3242,.T.);
#4440=EDGE_CURVE('',#3587,#3592,#2253,.T.);
#4441=EDGE_CURVE('',#3592,#3592,#3243,.T.);
#4442=EDGE_CURVE('',#3593,#3593,#3244,.T.);
#4443=EDGE_CURVE('',#3586,#3594,#2254,.T.);
#4444=EDGE_CURVE('',#3594,#3594,#3245,.T.);
#4445=EDGE_CURVE('',#3595,#3595,#3246,.T.);
#4446=EDGE_CURVE('',#3593,#3591,#2255,.T.);
#4447=EDGE_CURVE('',#3595,#3590,#2256,.T.);
#5875=ORIENTED_EDGE('',*,*,#4424,.F.);
#5876=ORIENTED_EDGE('',*,*,#4425,.F.);
#5877=ORIENTED_EDGE('',*,*,#4426,.F.);
#5878=ORIENTED_EDGE('',*,*,#4427,.F.);
#5879=ORIENTED_EDGE('',*,*,#4426,.T.);
#5880=ORIENTED_EDGE('',*,*,#4428,.T.);
#5881=ORIENTED_EDGE('',*,*,#4429,.T.);
#5882=ORIENTED_EDGE('',*,*,#4430,.F.);
#5883=ORIENTED_EDGE('',*,*,#4431,.T.);
#5884=ORIENTED_EDGE('',*,*,#4432,.T.);
#5885=ORIENTED_EDGE('',*,*,#4425,.T.);
#5886=ORIENTED_EDGE('',*,*,#4433,.F.);
#5887=ORIENTED_EDGE('',*,*,#4434,.T.);
#5888=ORIENTED_EDGE('',*,*,#4428,.F.);
#5889=ORIENTED_EDGE('',*,*,#4429,.F.);
#5890=ORIENTED_EDGE('',*,*,#4434,.F.);
#5891=ORIENTED_EDGE('',*,*,#4435,.F.);
#5892=ORIENTED_EDGE('',*,*,#4436,.F.);
#5893=ORIENTED_EDGE('',*,*,#4424,.T.);
#5894=ORIENTED_EDGE('',*,*,#4437,.F.);
#5895=ORIENTED_EDGE('',*,*,#4435,.T.);
#5896=ORIENTED_EDGE('',*,*,#4433,.T.);
#5897=ORIENTED_EDGE('',*,*,#4438,.T.);
#5898=ORIENTED_EDGE('',*,*,#4439,.T.);
#5899=ORIENTED_EDGE('',*,*,#4432,.F.);
#5900=ORIENTED_EDGE('',*,*,#4440,.T.);
#5901=ORIENTED_EDGE('',*,*,#4441,.T.);
#5902=ORIENTED_EDGE('',*,*,#4440,.F.);
#5903=ORIENTED_EDGE('',*,*,#4441,.F.);
#5904=ORIENTED_EDGE('',*,*,#4442,.F.);
#5905=ORIENTED_EDGE('',*,*,#4431,.F.);
#5906=ORIENTED_EDGE('',*,*,#4443,.T.);
#5907=ORIENTED_EDGE('',*,*,#4444,.T.);
#5908=ORIENTED_EDGE('',*,*,#4443,.F.);
#5909=ORIENTED_EDGE('',*,*,#4444,.F.);
#5910=ORIENTED_EDGE('',*,*,#4445,.F.);
#5911=ORIENTED_EDGE('',*,*,#4442,.T.);
#5912=ORIENTED_EDGE('',*,*,#4446,.T.);
#5913=ORIENTED_EDGE('',*,*,#4439,.F.);
#5914=ORIENTED_EDGE('',*,*,#4446,.F.);
#5915=ORIENTED_EDGE('',*,*,#4445,.T.);
#5916=ORIENTED_EDGE('',*,*,#4447,.T.);
#5917=ORIENTED_EDGE('',*,*,#4438,.F.);
#5918=ORIENTED_EDGE('',*,*,#4447,.F.);
#5919=ORIENTED_EDGE('',*,*,#4427,.T.);
#5920=ORIENTED_EDGE('',*,*,#4430,.T.);
#5921=ORIENTED_EDGE('',*,*,#4436,.T.);
#5922=ORIENTED_EDGE('',*,*,#4437,.T.);
#7400=CYLINDRICAL_SURFACE('',#8772,0.475);
#7401=CYLINDRICAL_SURFACE('',#8776,0.475);
#7402=CYLINDRICAL_SURFACE('',#8780,0.275);
#7403=CYLINDRICAL_SURFACE('',#8781,0.275);
#7759=ADVANCED_FACE('',(#1189),#919,.T.);
#7760=ADVANCED_FACE('',(#1190,#782,#783),#920,.T.);
#7761=ADVANCED_FACE('',(#1191),#921,.F.);
#7762=ADVANCED_FACE('',(#1192),#922,.F.);
#7763=ADVANCED_FACE('',(#1193,#784,#785),#923,.T.);
#7764=ADVANCED_FACE('',(#1194),#7400,.F.);
#7765=ADVANCED_FACE('',(#1195,#786),#924,.F.);
#7766=ADVANCED_FACE('',(#1196),#7401,.F.);
#7767=ADVANCED_FACE('',(#1197,#787),#925,.F.);
#7768=ADVANCED_FACE('',(#1198),#7402,.F.);
#7769=ADVANCED_FACE('',(#1199),#7403,.F.);
#7770=ADVANCED_FACE('',(#1200),#926,.T.);
#8075=CLOSED_SHELL('',(#7759,#7760,#7761,#7762,#7763,#7764,#7765,#7766,
#7767,#7768,#7769,#7770));
#8762=AXIS2_PLACEMENT_3D('',#12461,#10105,#10106);
#8763=AXIS2_PLACEMENT_3D('',#12462,#10107,#10108);
#8764=AXIS2_PLACEMENT_3D('',#12471,#10113,#10114);
#8765=AXIS2_PLACEMENT_3D('',#12478,#10118,#10119);
#8766=AXIS2_PLACEMENT_3D('',#12480,#10120,#10121);
#8767=AXIS2_PLACEMENT_3D('',#12481,#10122,#10123);
#8768=AXIS2_PLACEMENT_3D('',#12485,#10126,#10127);
#8769=AXIS2_PLACEMENT_3D('',#12489,#10130,#10131);
#8770=AXIS2_PLACEMENT_3D('',#12492,#10133,#10134);
#8771=AXIS2_PLACEMENT_3D('',#12494,#10135,#10136);
#8772=AXIS2_PLACEMENT_3D('',#12495,#10137,#10138);
#8773=AXIS2_PLACEMENT_3D('',#12498,#10140,#10141);
#8774=AXIS2_PLACEMENT_3D('',#12499,#10142,#10143);
#8775=AXIS2_PLACEMENT_3D('',#12501,#10144,#10145);
#8776=AXIS2_PLACEMENT_3D('',#12502,#10146,#10147);
#8777=AXIS2_PLACEMENT_3D('',#12505,#10149,#10150);
#8778=AXIS2_PLACEMENT_3D('',#12506,#10151,#10152);
#8779=AXIS2_PLACEMENT_3D('',#12508,#10153,#10154);
#8780=AXIS2_PLACEMENT_3D('',#12509,#10155,#10156);
#8781=AXIS2_PLACEMENT_3D('',#12511,#10158,#10159);
#8782=AXIS2_PLACEMENT_3D('',#12513,#10161,#10162);
#10105=DIRECTION('axis',(0.,0.,1.));
#10106=DIRECTION('refdir',(1.,0.,0.));
#10107=DIRECTION('center_axis',(0.,1.,0.));
#10108=DIRECTION('ref_axis',(1.,0.,0.));
#10109=DIRECTION('',(0.,0.,1.));
#10110=DIRECTION('',(1.,0.,0.));
#10111=DIRECTION('',(0.,0.,-1.));
#10112=DIRECTION('',(-1.,0.,0.));
#10113=DIRECTION('center_axis',(-1.,0.,0.));
#10114=DIRECTION('ref_axis',(0.,-1.,0.));
#10115=DIRECTION('',(0.,-1.,0.));
#10116=DIRECTION('',(0.,0.,1.));
#10117=DIRECTION('',(0.,-1.,0.));
#10118=DIRECTION('center_axis',(1.,0.,0.));
#10119=DIRECTION('ref_axis',(0.,0.,-1.));
#10120=DIRECTION('center_axis',(1.,0.,0.));
#10121=DIRECTION('ref_axis',(0.,0.,-1.));
#10122=DIRECTION('center_axis',(0.,0.,1.));
#10123=DIRECTION('ref_axis',(1.,0.,0.));
#10124=DIRECTION('',(0.,1.,0.));
#10125=DIRECTION('',(-1.,0.,0.));
#10126=DIRECTION('center_axis',(0.,1.,0.));
#10127=DIRECTION('ref_axis',(0.,0.,1.));
#10128=DIRECTION('',(0.,0.,-1.));
#10129=DIRECTION('',(1.,0.,0.));
#10130=DIRECTION('center_axis',(1.,0.,0.));
#10131=DIRECTION('ref_axis',(0.,1.,0.));
#10132=DIRECTION('',(0.,1.,0.));
#10133=DIRECTION('center_axis',(-1.,0.,0.));
#10134=DIRECTION('ref_axis',(0.,0.,-1.));
#10135=DIRECTION('center_axis',(-1.,0.,0.));
#10136=DIRECTION('ref_axis',(0.,0.,-1.));
#10137=DIRECTION('center_axis',(1.,0.,0.));
#10138=DIRECTION('ref_axis',(0.,0.,-1.));
#10139=DIRECTION('',(1.,0.,0.));
#10140=DIRECTION('center_axis',(1.,0.,0.));
#10141=DIRECTION('ref_axis',(0.,0.,-1.));
#10142=DIRECTION('center_axis',(1.,0.,0.));
#10143=DIRECTION('ref_axis',(0.,0.,-1.));
#10144=DIRECTION('center_axis',(-1.,0.,0.));
#10145=DIRECTION('ref_axis',(0.,0.,-1.));
#10146=DIRECTION('center_axis',(1.,0.,0.));
#10147=DIRECTION('ref_axis',(0.,0.,-1.));
#10148=DIRECTION('',(1.,0.,0.));
#10149=DIRECTION('center_axis',(1.,0.,0.));
#10150=DIRECTION('ref_axis',(0.,0.,-1.));
#10151=DIRECTION('center_axis',(1.,0.,0.));
#10152=DIRECTION('ref_axis',(0.,0.,-1.));
#10153=DIRECTION('center_axis',(-1.,0.,0.));
#10154=DIRECTION('ref_axis',(0.,0.,-1.));
#10155=DIRECTION('center_axis',(1.,0.,0.));
#10156=DIRECTION('ref_axis',(0.,0.,-1.));
#10157=DIRECTION('',(1.,0.,0.));
#10158=DIRECTION('center_axis',(1.,0.,0.));
#10159=DIRECTION('ref_axis',(0.,0.,-1.));
#10160=DIRECTION('',(1.,0.,0.));
#10161=DIRECTION('center_axis',(0.,0.,1.));
#10162=DIRECTION('ref_axis',(1.,0.,0.));
#12461=CARTESIAN_POINT('',(0.,0.,0.));
#12462=CARTESIAN_POINT('Origin',(14.95,3.75,5.));
#12463=CARTESIAN_POINT('',(11.,3.75,4.6));
#12464=CARTESIAN_POINT('',(11.,3.75,7.));
#12465=CARTESIAN_POINT('',(11.,3.75,4.8));
#12466=CARTESIAN_POINT('',(10.,3.75,4.6));
#12467=CARTESIAN_POINT('',(12.725,3.75,4.6));
#12468=CARTESIAN_POINT('',(10.,3.75,7.));
#12469=CARTESIAN_POINT('',(10.,3.75,4.8));
#12470=CARTESIAN_POINT('',(12.725,3.75,7.));
#12471=CARTESIAN_POINT('Origin',(10.,5.,4.6));
#12472=CARTESIAN_POINT('',(10.,-3.75,4.6));
#12473=CARTESIAN_POINT('',(10.,5.,4.6));
#12474=CARTESIAN_POINT('',(10.,-3.75,7.));
#12475=CARTESIAN_POINT('',(10.,-3.75,4.8));
#12476=CARTESIAN_POINT('',(10.,5.,7.));
#12477=CARTESIAN_POINT('',(10.,3.,6.275));
#12478=CARTESIAN_POINT('Origin',(10.,3.,5.8));
#12479=CARTESIAN_POINT('',(10.,-3.,6.275));
#12480=CARTESIAN_POINT('Origin',(10.,-3.,5.8));
#12481=CARTESIAN_POINT('Origin',(10.5,0.,4.6));
#12482=CARTESIAN_POINT('',(11.,-3.75,4.6));
#12483=CARTESIAN_POINT('',(11.,-5.,4.6));
#12484=CARTESIAN_POINT('',(12.725,-3.75,4.6));
#12485=CARTESIAN_POINT('Origin',(14.95,-3.75,5.));
#12486=CARTESIAN_POINT('',(11.,-3.75,7.));
#12487=CARTESIAN_POINT('',(11.,-3.75,4.8));
#12488=CARTESIAN_POINT('',(12.725,-3.75,7.));
#12489=CARTESIAN_POINT('Origin',(11.,-5.,4.6));
#12490=CARTESIAN_POINT('',(11.,-5.,7.));
#12491=CARTESIAN_POINT('',(11.,3.,6.075));
#12492=CARTESIAN_POINT('Origin',(11.,3.,5.8));
#12493=CARTESIAN_POINT('',(11.,-3.,6.075));
#12494=CARTESIAN_POINT('Origin',(11.,-3.,5.8));
#12495=CARTESIAN_POINT('Origin',(9.9,-3.,5.8));
#12496=CARTESIAN_POINT('',(10.55,-3.,6.275));
#12497=CARTESIAN_POINT('',(9.9,-3.,6.275));
#12498=CARTESIAN_POINT('Origin',(10.55,-3.,5.8));
#12499=CARTESIAN_POINT('Origin',(10.55,-3.,5.8));
#12500=CARTESIAN_POINT('',(10.55,-3.,6.075));
#12501=CARTESIAN_POINT('Origin',(10.55,-3.,5.8));
#12502=CARTESIAN_POINT('Origin',(9.9,3.,5.8));
#12503=CARTESIAN_POINT('',(10.55,3.,6.275));
#12504=CARTESIAN_POINT('',(9.9,3.,6.275));
#12505=CARTESIAN_POINT('Origin',(10.55,3.,5.8));
#12506=CARTESIAN_POINT('Origin',(10.55,3.,5.8));
#12507=CARTESIAN_POINT('',(10.55,3.,6.075));
#12508=CARTESIAN_POINT('Origin',(10.55,3.,5.8));
#12509=CARTESIAN_POINT('Origin',(9.9,-3.,5.8));
#12510=CARTESIAN_POINT('',(9.9,-3.,6.075));
#12511=CARTESIAN_POINT('Origin',(9.9,3.,5.8));
#12512=CARTESIAN_POINT('',(9.9,3.,6.075));
#12513=CARTESIAN_POINT('Origin',(10.5,0.,7.));
#25025=UNCERTAINTY_MEASURE_WITH_UNIT(LENGTH_MEASURE(0.001),#25075,
'DISTANCE_ACCURACY_VALUE',
'Maximum model space distance between geometric entities at asserted c
onnectivities');
#25040=UNCERTAINTY_MEASURE_WITH_UNIT(LENGTH_MEASURE(0.001),#25075,
'DISTANCE_ACCURACY_VALUE',
'Maximum model space distance between geometric entities at asserted c
onnectivities');
#25059=(
GEOMETRIC_REPRESENTATION_CONTEXT(3)
GLOBAL_UNCERTAINTY_ASSIGNED_CONTEXT((#25025))
GLOBAL_UNIT_ASSIGNED_CONTEXT((#25075,#25077,#25078))
REPRESENTATION_CONTEXT('','3D')
);
#25074=(
GEOMETRIC_REPRESENTATION_CONTEXT(3)
GLOBAL_UNCERTAINTY_ASSIGNED_CONTEXT((#25040))
GLOBAL_UNIT_ASSIGNED_CONTEXT((#25075,#25077,#25078))
REPRESENTATION_CONTEXT('','3D')
);
#25075=(
LENGTH_UNIT()
NAMED_UNIT(*)
SI_UNIT(.CENTI.,.METRE.)
);
#25077=(
NAMED_UNIT(*)
PLANE_ANGLE_UNIT()
SI_UNIT($,.RADIAN.)
);
#25078=(
NAMED_UNIT(*)
SI_UNIT($,.STERADIAN.)
SOLID_ANGLE_UNIT()
);
#25097=SHAPE_DEFINITION_REPRESENTATION(#25135,#25212);
#25135=PRODUCT_DEFINITION_SHAPE('',$,#25246);
#25212=SHAPE_REPRESENTATION('',(#8762),#25059);
#25227=PRODUCT_DEFINITION_CONTEXT('part definition',#25328,'design');
#25246=PRODUCT_DEFINITION('Seventy-five millimetre jaw insert (1)',
'Seventy-five millimetre jaw insert (1)',#25279,#25227);
#25279=PRODUCT_DEFINITION_FORMATION('',$,#25348);
#25328=APPLICATION_CONTEXT(
'Core Data for Automotive Mechanical Design Process');
#25329=PRODUCT_CONTEXT('part definition',#25328,'mechanical');
#25348=PRODUCT('Seventy-five millimetre jaw insert (1)',
'Seventy-five millimetre jaw insert (1)',
'Seventy-five millimetre jaw insert (1)',(#25329));
#25447=COLOUR_RGB('Off White',0.89,0.88,0.83);
#25448=FILL_AREA_STYLE_COLOUR('',#25447);
#25449=FILL_AREA_STYLE('',(#25448));
#25450=SURFACE_STYLE_FILL_AREA(#25449);
#25451=SURFACE_SIDE_STYLE('',(#25450));
#25452=SURFACE_STYLE_USAGE(.BOTH.,#25451);
#25453=PRESENTATION_STYLE_ASSIGNMENT((#25452));
ENDSEC;
END-ISO-10303-21;
